ISO-10303-21;
HEADER;
/* Generated by software containing ST-Developer
 * from STEP Tools, Inc. (www.steptools.com) 
 */

FILE_DESCRIPTION(
/* description */ ('Rigid flange shaft coupling assembly'),
/* implementation_level */ '2;1');

FILE_NAME(
/* name */ 'End collar (1).step',
/* time_stamp */ '2026-10-27T10:47:16-07:00',
/* author */ (''),
/* organization */ (''),
/* preprocessor_version */ 'ST-DEVELOPER v20.2',
/* originating_system */ 'Autodesk Translation Framework v15.17.0.0',
/* authorisation */ '');

FILE_SCHEMA (('AUTOMOTIVE_DESIGN { 1 0 10303 214 3 1 1 }'));
ENDSEC;

DATA;
#10=MECHANICAL_DESIGN_GEOMETRIC_PRESENTATION_REPRESENTATION('',(#420),#9141);
#336=B_SPLINE_CURVE_WITH_KNOTS('',3,(#8590,#8591,#8592,#8593,#8594,#8595,
#8596,#8597,#8598,#8599,#8600,#8601,#8602,#8603),.UNSPECIFIED.,.F.,.F.,
(4,2,2,2,2,2,4),(0.756005737987019,0.793568827564645,0.8729225200542,0.952276212543755,
1.03162990503331,1.11098359752287,1.14854668710049),.UNSPECIFIED.);
#337=B_SPLINE_CURVE_WITH_KNOTS('',3,(#8609,#8610,#8611,#8612,#8613,#8614,
#8615,#8616,#8617,#8618,#8619,#8620,#8621,#8622,#8623,#8624,#8625,#8626),
 .UNSPECIFIED.,.F.,.F.,(4,2,2,2,2,2,2,2,4),(0.,0.0792165807733624,0.158433161546725,
0.23764869707457,0.316864232602414,0.396079768130259,0.475295303658103,
0.554511884431466,0.633728465204828),.UNSPECIFIED.);
#338=B_SPLINE_CURVE_WITH_KNOTS('',3,(#8627,#8628,#8629,#8630,#8631,#8632,
#8633,#8634,#8635,#8636,#8637,#8638,#8639,#8640,#8641,#8642,#8643,#8644),
 .UNSPECIFIED.,.F.,.F.,(4,2,2,2,2,2,2,2,4),(0.633728465204828,0.712945045978191,
0.792161626751553,0.871377162279398,0.950592697807242,1.02980823333509,
1.10902376886293,1.18824034963629,1.26745693040966),.UNSPECIFIED.);
#339=B_SPLINE_CURVE_WITH_KNOTS('',3,(#8647,#8648,#8649,#8650,#8651,#8652,
#8653,#8654,#8655,#8656,#8657,#8658,#8659,#8660),.UNSPECIFIED.,.F.,.F.,
(4,2,2,2,2,2,4),(0.121154929624521,0.158718019202141,0.238071711691696,
0.317425404181252,0.396779096670807,0.476132789160362,0.513695878737985),
 .UNSPECIFIED.);
#363=SHAPE_REPRESENTATION_RELATIONSHIP('SRR','None',#9299,#391);
#391=ADVANCED_BREP_SHAPE_REPRESENTATION('',(#448),#9134);
#420=STYLED_ITEM('',(#9486),#448);
#448=MANIFOLD_SOLID_BREP('Body1',#4775);
#559=FACE_BOUND('',#1320,.T.);
#560=FACE_BOUND('',#1322,.T.);
#561=FACE_BOUND('',#1324,.T.);
#562=FACE_BOUND('',#1326,.T.);
#689=PLANE('',#5461);
#690=PLANE('',#5466);
#691=PLANE('',#5473);
#692=PLANE('',#5474);
#938=FACE_OUTER_BOUND('',#1316,.T.);
#939=FACE_OUTER_BOUND('',#1317,.T.);
#940=FACE_OUTER_BOUND('',#1318,.T.);
#941=FACE_OUTER_BOUND('',#1319,.T.);
#942=FACE_OUTER_BOUND('',#1321,.T.);
#943=FACE_OUTER_BOUND('',#1323,.T.);
#944=FACE_OUTER_BOUND('',#1325,.T.);
#1316=EDGE_LOOP('',(#4079,#4080));
#1317=EDGE_LOOP('',(#4081,#4082,#4083,#4084,#4085,#4086,#4087,#4088,#4089));
#1318=EDGE_LOOP('',(#4090,#4091,#4092));
#1319=EDGE_LOOP('',(#4093,#4094,#4095,#4096));
#1320=EDGE_LOOP('',(#4097,#4098,#4099,#4100));
#1321=EDGE_LOOP('',(#4101,#4102,#4103,#4104));
#1322=EDGE_LOOP('',(#4105,#4106));
#1323=EDGE_LOOP('',(#4107));
#1324=EDGE_LOOP('',(#4108));
#1325=EDGE_LOOP('',(#4109));
#1326=EDGE_LOOP('',(#4110));
#1641=LINE('',#8586,#1986);
#1642=LINE('',#8607,#1987);
#1643=LINE('',#8662,#1988);
#1644=LINE('',#8667,#1989);
#1645=LINE('',#8673,#1990);
#1986=VECTOR('',#6616,1.);
#1987=VECTOR('',#6623,0.21);
#1988=VECTOR('',#6628,1.);
#1989=VECTOR('',#6633,1.005);
#1990=VECTOR('',#6640,1.5);
#2241=CIRCLE('',#5462,0.21);
#2242=CIRCLE('',#5464,0.21);
#2243=CIRCLE('',#5465,0.21);
#2244=CIRCLE('',#5468,1.005);
#2245=CIRCLE('',#5469,1.005);
#2246=CIRCLE('',#5471,1.5);
#2247=CIRCLE('',#5472,1.5);
#2562=VERTEX_POINT('',#8584);
#2563=VERTEX_POINT('',#8585);
#2564=VERTEX_POINT('',#8589);
#2565=VERTEX_POINT('',#8604);
#2566=VERTEX_POINT('',#8606);
#2567=VERTEX_POINT('',#8608);
#2568=VERTEX_POINT('',#8645);
#2569=VERTEX_POINT('',#8664);
#2570=VERTEX_POINT('',#8666);
#2571=VERTEX_POINT('',#8670);
#2572=VERTEX_POINT('',#8672);
#3083=EDGE_CURVE('',#2562,#2563,#1641,.T.);
#3084=EDGE_CURVE('',#2562,#2563,#2241,.T.);
#3085=EDGE_CURVE('',#2564,#2562,#336,.T.);
#3086=EDGE_CURVE('',#2565,#2564,#2242,.T.);
#3087=EDGE_CURVE('',#2565,#2566,#1642,.T.);
#3088=EDGE_CURVE('',#2567,#2566,#337,.T.);
#3089=EDGE_CURVE('',#2566,#2567,#338,.T.);
#3090=EDGE_CURVE('',#2568,#2565,#2243,.T.);
#3091=EDGE_CURVE('',#2563,#2568,#339,.T.);
#3092=EDGE_CURVE('',#2568,#2564,#1643,.T.);
#3093=EDGE_CURVE('',#2569,#2569,#2244,.T.);
#3094=EDGE_CURVE('',#2569,#2570,#1644,.T.);
#3095=EDGE_CURVE('',#2570,#2570,#2245,.T.);
#3096=EDGE_CURVE('',#2571,#2571,#2246,.T.);
#3097=EDGE_CURVE('',#2571,#2572,#1645,.T.);
#3098=EDGE_CURVE('',#2572,#2572,#2247,.T.);
#4079=ORIENTED_EDGE('',*,*,#3083,.F.);
#4080=ORIENTED_EDGE('',*,*,#3084,.T.);
#4081=ORIENTED_EDGE('',*,*,#3085,.F.);
#4082=ORIENTED_EDGE('',*,*,#3086,.F.);
#4083=ORIENTED_EDGE('',*,*,#3087,.T.);
#4084=ORIENTED_EDGE('',*,*,#3088,.F.);
#4085=ORIENTED_EDGE('',*,*,#3089,.F.);
#4086=ORIENTED_EDGE('',*,*,#3087,.F.);
#4087=ORIENTED_EDGE('',*,*,#3090,.F.);
#4088=ORIENTED_EDGE('',*,*,#3091,.F.);
#4089=ORIENTED_EDGE('',*,*,#3084,.F.);
#4090=ORIENTED_EDGE('',*,*,#3092,.F.);
#4091=ORIENTED_EDGE('',*,*,#3090,.T.);
#4092=ORIENTED_EDGE('',*,*,#3086,.T.);
#4093=ORIENTED_EDGE('',*,*,#3093,.F.);
#4094=ORIENTED_EDGE('',*,*,#3094,.T.);
#4095=ORIENTED_EDGE('',*,*,#3095,.T.);
#4096=ORIENTED_EDGE('',*,*,#3094,.F.);
#4097=ORIENTED_EDGE('',*,*,#3091,.T.);
#4098=ORIENTED_EDGE('',*,*,#3092,.T.);
#4099=ORIENTED_EDGE('',*,*,#3085,.T.);
#4100=ORIENTED_EDGE('',*,*,#3083,.T.);
#4101=ORIENTED_EDGE('',*,*,#3096,.F.);
#4102=ORIENTED_EDGE('',*,*,#3097,.T.);
#4103=ORIENTED_EDGE('',*,*,#3098,.T.);
#4104=ORIENTED_EDGE('',*,*,#3097,.F.);
#4105=ORIENTED_EDGE('',*,*,#3088,.T.);
#4106=ORIENTED_EDGE('',*,*,#3089,.T.);
#4107=ORIENTED_EDGE('',*,*,#3096,.T.);
#4108=ORIENTED_EDGE('',*,*,#3093,.T.);
#4109=ORIENTED_EDGE('',*,*,#3098,.F.);
#4110=ORIENTED_EDGE('',*,*,#3095,.F.);
#4469=CYLINDRICAL_SURFACE('',#5463,0.21);
#4470=CYLINDRICAL_SURFACE('',#5467,1.005);
#4471=CYLINDRICAL_SURFACE('',#5470,1.5);
#4674=ADVANCED_FACE('',(#938),#689,.T.);
#4675=ADVANCED_FACE('',(#939),#4469,.F.);
#4676=ADVANCED_FACE('',(#940),#690,.T.);
#4677=ADVANCED_FACE('',(#941,#559),#4470,.F.);
#4678=ADVANCED_FACE('',(#942,#560),#4471,.T.);
#4679=ADVANCED_FACE('',(#943,#561),#691,.T.);
#4680=ADVANCED_FACE('',(#944,#562),#692,.F.);
#4775=CLOSED_SHELL('',(#4674,#4675,#4676,#4677,#4678,#4679,#4680));
#5460=AXIS2_PLACEMENT_3D('',#8582,#6612,#6613);
#5461=AXIS2_PLACEMENT_3D('',#8583,#6614,#6615);
#5462=AXIS2_PLACEMENT_3D('',#8587,#6617,#6618);
#5463=AXIS2_PLACEMENT_3D('',#8588,#6619,#6620);
#5464=AXIS2_PLACEMENT_3D('',#8605,#6621,#6622);
#5465=AXIS2_PLACEMENT_3D('',#8646,#6624,#6625);
#5466=AXIS2_PLACEMENT_3D('',#8661,#6626,#6627);
#5467=AXIS2_PLACEMENT_3D('',#8663,#6629,#6630);
#5468=AXIS2_PLACEMENT_3D('',#8665,#6631,#6632);
#5469=AXIS2_PLACEMENT_3D('',#8668,#6634,#6635);
#5470=AXIS2_PLACEMENT_3D('',#8669,#6636,#6637);
#5471=AXIS2_PLACEMENT_3D('',#8671,#6638,#6639);
#5472=AXIS2_PLACEMENT_3D('',#8674,#6641,#6642);
#5473=AXIS2_PLACEMENT_3D('',#8675,#6643,#6644);
#5474=AXIS2_PLACEMENT_3D('',#8676,#6645,#6646);
#6612=DIRECTION('axis',(0.,0.,1.));
#6613=DIRECTION('refdir',(1.,0.,0.));
#6614=DIRECTION('center_axis',(0.,0.,1.));
#6615=DIRECTION('ref_axis',(1.,0.,0.));
#6616=DIRECTION('',(0.,1.,0.));
#6617=DIRECTION('center_axis',(0.,0.,1.));
#6618=DIRECTION('ref_axis',(1.,0.,0.));
#6619=DIRECTION('center_axis',(0.,0.,1.));
#6620=DIRECTION('ref_axis',(1.,0.,0.));
#6621=DIRECTION('center_axis',(0.,0.,1.));
#6622=DIRECTION('ref_axis',(1.,0.,0.));
#6623=DIRECTION('',(0.,0.,1.));
#6624=DIRECTION('center_axis',(0.,0.,1.));
#6625=DIRECTION('ref_axis',(1.,0.,0.));
#6626=DIRECTION('center_axis',(0.,0.,1.));
#6627=DIRECTION('ref_axis',(1.,0.,0.));
#6628=DIRECTION('',(0.,-1.,0.));
#6629=DIRECTION('center_axis',(0.,1.,0.));
#6630=DIRECTION('ref_axis',(1.,0.,0.));
#6631=DIRECTION('center_axis',(0.,-1.,0.));
#6632=DIRECTION('ref_axis',(1.,0.,0.));
#6633=DIRECTION('',(0.,-1.,0.));
#6634=DIRECTION('center_axis',(0.,-1.,0.));
#6635=DIRECTION('ref_axis',(1.,0.,0.));
#6636=DIRECTION('center_axis',(0.,1.,0.));
#6637=DIRECTION('ref_axis',(1.,0.,0.));
#6638=DIRECTION('center_axis',(0.,1.,0.));
#6639=DIRECTION('ref_axis',(1.,0.,0.));
#6640=DIRECTION('',(0.,-1.,0.));
#6641=DIRECTION('center_axis',(0.,1.,0.));
#6642=DIRECTION('ref_axis',(1.,0.,0.));
#6643=DIRECTION('center_axis',(0.,1.,0.));
#6644=DIRECTION('ref_axis',(1.,0.,0.));
#6645=DIRECTION('center_axis',(0.,1.,0.));
#6646=DIRECTION('ref_axis',(1.,0.,0.));
#8582=CARTESIAN_POINT('',(0.,0.,0.));
#8583=CARTESIAN_POINT('Origin',(0.,22.85,7.52));
#8584=CARTESIAN_POINT('',(0.172988438920056,22.7309411910021,7.52));
#8585=CARTESIAN_POINT('',(0.172988438920056,22.9690588089979,7.52));
#8586=CARTESIAN_POINT('',(0.172988438920056,22.45,7.52));
#8587=CARTESIAN_POINT('Origin',(0.,22.85,7.52));
#8588=CARTESIAN_POINT('Origin',(0.,22.85,7.52));
#8589=CARTESIAN_POINT('',(-0.172988438920056,22.7309411910021,7.52));
#8590=CARTESIAN_POINT('Ctrl Pts',(-0.172988438920056,22.7309411910021,7.52));
#8591=CARTESIAN_POINT('Ctrl Pts',(-0.165594865311315,22.7201985776047,7.52129192197638));
#8592=CARTESIAN_POINT('Ctrl Pts',(-0.157297138725606,22.7103122906273,7.52265394943905));
#8593=CARTESIAN_POINT('Ctrl Pts',(-0.129892073845076,22.6829072257467,7.5267480843909));
#8594=CARTESIAN_POINT('Ctrl Pts',(-0.106330167759284,22.6667579436671,7.52969589327638));
#8595=CARTESIAN_POINT('Ctrl Pts',(-0.0546129046324105,22.6453022060351,
7.53385029472357));
#8596=CARTESIAN_POINT('Ctrl Pts',(-0.0264512308298518,22.64,7.535));
#8597=CARTESIAN_POINT('Ctrl Pts',(0.0264512308298517,22.64,7.535));
#8598=CARTESIAN_POINT('Ctrl Pts',(0.0546129046324104,22.6453022060351,7.53385029472357));
#8599=CARTESIAN_POINT('Ctrl Pts',(0.106330167759284,22.6667579436671,7.52969589327638));
#8600=CARTESIAN_POINT('Ctrl Pts',(0.129892073845076,22.6829072257467,7.5267480843909));
#8601=CARTESIAN_POINT('Ctrl Pts',(0.157297138725606,22.7103122906273,7.52265394943905));
#8602=CARTESIAN_POINT('Ctrl Pts',(0.165594865311316,22.7201985776047,7.52129192197638));
#8603=CARTESIAN_POINT('Ctrl Pts',(0.172988438920057,22.7309411910021,7.52));
#8604=CARTESIAN_POINT('',(-0.21,22.85,7.52));
#8605=CARTESIAN_POINT('Origin',(0.,22.85,7.52));
#8606=CARTESIAN_POINT('',(-0.21,22.85,8.01522725533839));
#8607=CARTESIAN_POINT('',(-0.21,22.85,7.52));
#8608=CARTESIAN_POINT('',(0.21,22.85,8.01522725533839));
#8609=CARTESIAN_POINT('Ctrl Pts',(0.21,22.85,8.01522725533839));
#8610=CARTESIAN_POINT('Ctrl Pts',(0.21,22.8235944730755,8.01522725533839));
#8611=CARTESIAN_POINT('Ctrl Pts',(0.204715737269595,22.7954529259093,8.01600415954412));
#8612=CARTESIAN_POINT('Ctrl Pts',(0.18327376303633,22.7437237310949,8.01880073282317));
#8613=CARTESIAN_POINT('Ctrl Pts',(0.167117923970393,22.720133075872,8.02077897157582));
#8614=CARTESIAN_POINT('Ctrl Pts',(0.129867169887369,22.682882321789,8.02448481141327));
#8615=CARTESIAN_POINT('Ctrl Pts',(0.106276408305767,22.6667262899986,8.02645455657129));
#8616=CARTESIAN_POINT('Ctrl Pts',(0.0545468514059018,22.6452841751738,8.02923165515645));
#8617=CARTESIAN_POINT('Ctrl Pts',(0.0264051785092816,22.64,8.03));
#8618=CARTESIAN_POINT('Ctrl Pts',(-0.0264051785092815,22.64,8.03));
#8619=CARTESIAN_POINT('Ctrl Pts',(-0.0545468514059018,22.6452841751738,
8.02923165515645));
#8620=CARTESIAN_POINT('Ctrl Pts',(-0.106276408305767,22.6667262899986,8.02645455657129));
#8621=CARTESIAN_POINT('Ctrl Pts',(-0.129867169887368,22.682882321789,8.02448481141327));
#8622=CARTESIAN_POINT('Ctrl Pts',(-0.167117923970393,22.720133075872,8.02077897157582));
#8623=CARTESIAN_POINT('Ctrl Pts',(-0.183273763036334,22.7437237310949,8.01880073282317));
#8624=CARTESIAN_POINT('Ctrl Pts',(-0.204715737269597,22.7954529259093,8.01600415954412));
#8625=CARTESIAN_POINT('Ctrl Pts',(-0.21,22.8235944730755,8.01522725533839));
#8626=CARTESIAN_POINT('Ctrl Pts',(-0.21,22.85,8.01522725533839));
#8627=CARTESIAN_POINT('Ctrl Pts',(-0.21,22.85,8.01522725533839));
#8628=CARTESIAN_POINT('Ctrl Pts',(-0.21,22.8764055269245,8.01522725533839));
#8629=CARTESIAN_POINT('Ctrl Pts',(-0.204715737269595,22.9045470740907,8.01600415954412));
#8630=CARTESIAN_POINT('Ctrl Pts',(-0.18327376303633,22.9562762689051,8.01880073282317));
#8631=CARTESIAN_POINT('Ctrl Pts',(-0.167117923970393,22.979866924128,8.02077897157582));
#8632=CARTESIAN_POINT('Ctrl Pts',(-0.129867169887369,23.017117678211,8.02448481141327));
#8633=CARTESIAN_POINT('Ctrl Pts',(-0.106276408305767,23.0332737100014,8.02645455657129));
#8634=CARTESIAN_POINT('Ctrl Pts',(-0.0545468514059018,23.0547158248262,
8.02923165515645));
#8635=CARTESIAN_POINT('Ctrl Pts',(-0.0264051785092816,23.06,8.03));
#8636=CARTESIAN_POINT('Ctrl Pts',(0.0264051785092815,23.06,8.03));
#8637=CARTESIAN_POINT('Ctrl Pts',(0.0545468514059019,23.0547158248262,8.02923165515645));
#8638=CARTESIAN_POINT('Ctrl Pts',(0.106276408305767,23.0332737100014,8.02645455657129));
#8639=CARTESIAN_POINT('Ctrl Pts',(0.129867169887368,23.017117678211,8.02448481141327));
#8640=CARTESIAN_POINT('Ctrl Pts',(0.167117923970393,22.979866924128,8.02077897157582));
#8641=CARTESIAN_POINT('Ctrl Pts',(0.18327376303633,22.9562762689051,8.01880073282317));
#8642=CARTESIAN_POINT('Ctrl Pts',(0.204715737269595,22.9045470740907,8.01600415954412));
#8643=CARTESIAN_POINT('Ctrl Pts',(0.21,22.8764055269245,8.01522725533839));
#8644=CARTESIAN_POINT('Ctrl Pts',(0.21,22.85,8.01522725533839));
#8645=CARTESIAN_POINT('',(-0.172988438920056,22.9690588089979,7.52));
#8646=CARTESIAN_POINT('Origin',(0.,22.85,7.52));
#8647=CARTESIAN_POINT('Ctrl Pts',(0.172988438920055,22.9690588089979,7.52));
#8648=CARTESIAN_POINT('Ctrl Pts',(0.165594865311314,22.9798014223953,7.52129192197638));
#8649=CARTESIAN_POINT('Ctrl Pts',(0.157297138725605,22.9896877093727,7.52265394943905));
#8650=CARTESIAN_POINT('Ctrl Pts',(0.129892073845076,23.0170927742533,7.5267480843909));
#8651=CARTESIAN_POINT('Ctrl Pts',(0.106330167759284,23.033242056333,7.52969589327638));
#8652=CARTESIAN_POINT('Ctrl Pts',(0.0546129046324105,23.0546977939649,7.53385029472357));
#8653=CARTESIAN_POINT('Ctrl Pts',(0.0264512308298518,23.06,7.535));
#8654=CARTESIAN_POINT('Ctrl Pts',(-0.0264512308298517,23.06,7.535));
#8655=CARTESIAN_POINT('Ctrl Pts',(-0.0546129046324079,23.0546977939649,
7.53385029472357));
#8656=CARTESIAN_POINT('Ctrl Pts',(-0.106330167759282,23.033242056333,7.52969589327638));
#8657=CARTESIAN_POINT('Ctrl Pts',(-0.129892073845076,23.0170927742533,7.5267480843909));
#8658=CARTESIAN_POINT('Ctrl Pts',(-0.157297138725605,22.9896877093727,7.52265394943905));
#8659=CARTESIAN_POINT('Ctrl Pts',(-0.165594865311314,22.9798014223953,7.52129192197638));
#8660=CARTESIAN_POINT('Ctrl Pts',(-0.172988438920055,22.9690588089979,7.52));
#8661=CARTESIAN_POINT('Origin',(0.,22.85,7.52));
#8662=CARTESIAN_POINT('',(-0.172988438920056,22.45,7.52));
#8663=CARTESIAN_POINT('Origin',(0.,22.45,6.53));
#8664=CARTESIAN_POINT('',(-1.005,23.25,6.53));
#8665=CARTESIAN_POINT('Origin',(0.,23.25,6.53));
#8666=CARTESIAN_POINT('',(-1.005,22.45,6.53));
#8667=CARTESIAN_POINT('',(-1.005,22.45,6.53));
#8668=CARTESIAN_POINT('Origin',(0.,22.45,6.53));
#8669=CARTESIAN_POINT('Origin',(0.,22.45,6.53));
#8670=CARTESIAN_POINT('',(-1.5,23.25,6.53));
#8671=CARTESIAN_POINT('Origin',(0.,23.25,6.53));
#8672=CARTESIAN_POINT('',(-1.5,22.45,6.53));
#8673=CARTESIAN_POINT('',(-1.5,22.45,6.53));
#8674=CARTESIAN_POINT('Origin',(0.,22.45,6.53));
#8675=CARTESIAN_POINT('Origin',(0.,23.25,6.53));
#8676=CARTESIAN_POINT('Origin',(0.,22.45,6.53));
#9101=UNCERTAINTY_MEASURE_WITH_UNIT(LENGTH_MEASURE(0.001),#9142,
'DISTANCE_ACCURACY_VALUE',
'Maximum model space distance between geometric entities at asserted c
onnectivities');
#9108=UNCERTAINTY_MEASURE_WITH_UNIT(LENGTH_MEASURE(0.001),#9142,
'DISTANCE_ACCURACY_VALUE',
'Maximum model space distance between geometric entities at asserted c
onnectivities');
#9134=(
GEOMETRIC_REPRESENTATION_CONTEXT(3)
GLOBAL_UNCERTAINTY_ASSIGNED_CONTEXT((#9101))
GLOBAL_UNIT_ASSIGNED_CONTEXT((#9142,#9144,#9145))
REPRESENTATION_CONTEXT('','3D')
);
#9141=(
GEOMETRIC_REPRESENTATION_CONTEXT(3)
GLOBAL_UNCERTAINTY_ASSIGNED_CONTEXT((#9108))
GLOBAL_UNIT_ASSIGNED_CONTEXT((#9142,#9144,#9145))
REPRESENTATION_CONTEXT('','3D')
);
#9142=(
LENGTH_UNIT()
NAMED_UNIT(*)
SI_UNIT(.CENTI.,.METRE.)
);
#9144=(
NAMED_UNIT(*)
PLANE_ANGLE_UNIT()
SI_UNIT($,.RADIAN.)
);
#9145=(
NAMED_UNIT(*)
SI_UNIT($,.STERADIAN.)
SOLID_ANGLE_UNIT()
);
#9171=SHAPE_DEFINITION_REPRESENTATION(#9205,#9299);
#9205=PRODUCT_DEFINITION_SHAPE('',$,#9332);
#9299=SHAPE_REPRESENTATION('',(#5460),#9134);
#9306=PRODUCT_DEFINITION_CONTEXT('part definition',#9404,'design');
#9332=PRODUCT_DEFINITION('End collar (1)','End collar (1)',#9364,#9306);
#9364=PRODUCT_DEFINITION_FORMATION('',$,#9431);
#9404=APPLICATION_CONTEXT(
'Core Data for Automotive Mechanical Design Process');
#9405=PRODUCT_CONTEXT('part definition',#9404,'mechanical');
#9431=PRODUCT('End collar (1)','End collar (1)','End collar (1)',(#9405));
#9480=COLOUR_RGB('Light Blue',0.38,0.62,0.78);
#9481=FILL_AREA_STYLE_COLOUR('',#9480);
#9482=FILL_AREA_STYLE('',(#9481));
#9483=SURFACE_STYLE_FILL_AREA(#9482);
#9484=SURFACE_SIDE_STYLE('',(#9483));
#9485=SURFACE_STYLE_USAGE(.BOTH.,#9484);
#9486=PRESENTATION_STYLE_ASSIGNMENT((#9485));
ENDSEC;
END-ISO-10303-21;
